ISO-10303-21;
HEADER;
/* Generated by software containing ST-Developer
 * from STEP Tools, Inc. (www.steptools.com) 
 */

FILE_DESCRIPTION(
/* description */ (''),
/* implementation_level */ '2;1');

FILE_NAME(
/* name */ 'Bracket_03.step',
/* time_stamp */ '2026-10-22T16:03:28+06:00',
/* author */ (''),
/* organization */ (''),
/* preprocessor_version */ 'ST-DEVELOPER v20.2',
/* originating_system */ 'Autodesk Translation Framework v15.15.0.0',
/* authorisation */ '');

FILE_SCHEMA (('AUTOMOTIVE_DESIGN { 1 0 10303 214 3 1 1 }'));
ENDSEC;

DATA;
#10=MECHANICAL_DESIGN_GEOMETRIC_PRESENTATION_REPRESENTATION('',(#93),#6096);
#71=SHAPE_REPRESENTATION_RELATIONSHIP('SRR','None',#6146,#82);
#82=ADVANCED_BREP_SHAPE_REPRESENTATION('',(#104),#6094);
#93=STYLED_ITEM('',(#6234),#104);
#104=MANIFOLD_SOLID_BREP('Bracket_03',#3602);
#142=FACE_BOUND('',#693,.T.);
#143=FACE_BOUND('',#694,.T.);
#144=FACE_BOUND('',#695,.T.);
#145=FACE_BOUND('',#696,.T.);
#146=FACE_BOUND('',#698,.T.);
#147=FACE_BOUND('',#699,.T.);
#148=FACE_BOUND('',#700,.T.);
#149=FACE_BOUND('',#701,.T.);
#274=PLANE('',#3995);
#275=PLANE('',#3996);
#276=PLANE('',#3997);
#277=PLANE('',#3998);
#278=PLANE('',#3999);
#279=PLANE('',#4000);
#280=PLANE('',#4001);
#281=PLANE('',#4002);
#282=PLANE('',#4003);
#283=PLANE('',#4004);
#284=PLANE('',#4005);
#285=PLANE('',#4006);
#454=FACE_OUTER_BOUND('',#678,.T.);
#455=FACE_OUTER_BOUND('',#679,.T.);
#456=FACE_OUTER_BOUND('',#680,.T.);
#457=FACE_OUTER_BOUND('',#681,.T.);
#458=FACE_OUTER_BOUND('',#682,.T.);
#459=FACE_OUTER_BOUND('',#683,.T.);
#460=FACE_OUTER_BOUND('',#684,.T.);
#461=FACE_OUTER_BOUND('',#685,.T.);
#462=FACE_OUTER_BOUND('',#686,.T.);
#463=FACE_OUTER_BOUND('',#687,.T.);
#464=FACE_OUTER_BOUND('',#688,.T.);
#465=FACE_OUTER_BOUND('',#689,.T.);
#466=FACE_OUTER_BOUND('',#690,.T.);
#467=FACE_OUTER_BOUND('',#691,.T.);
#468=FACE_OUTER_BOUND('',#692,.T.);
#469=FACE_OUTER_BOUND('',#697,.T.);
#678=EDGE_LOOP('',(#3196,#3197,#3198,#3199));
#679=EDGE_LOOP('',(#3200,#3201,#3202,#3203));
#680=EDGE_LOOP('',(#3204,#3205,#3206,#3207));
#681=EDGE_LOOP('',(#3208,#3209,#3210,#3211));
#682=EDGE_LOOP('',(#3212,#3213,#3214,#3215));
#683=EDGE_LOOP('',(#3216,#3217,#3218,#3219));
#684=EDGE_LOOP('',(#3220,#3221,#3222,#3223));
#685=EDGE_LOOP('',(#3224,#3225,#3226,#3227));
#686=EDGE_LOOP('',(#3228,#3229,#3230,#3231));
#687=EDGE_LOOP('',(#3232,#3233,#3234,#3235));
#688=EDGE_LOOP('',(#3236,#3237,#3238,#3239));
#689=EDGE_LOOP('',(#3240,#3241,#3242,#3243));
#690=EDGE_LOOP('',(#3244,#3245,#3246,#3247));
#691=EDGE_LOOP('',(#3248,#3249,#3250,#3251));
#692=EDGE_LOOP('',(#3252,#3253,#3254,#3255,#3256,#3257,#3258,#3259,#3260,
#3261));
#693=EDGE_LOOP('',(#3262));
#694=EDGE_LOOP('',(#3263));
#695=EDGE_LOOP('',(#3264));
#696=EDGE_LOOP('',(#3265));
#697=EDGE_LOOP('',(#3266,#3267,#3268,#3269,#3270,#3271,#3272,#3273,#3274,
#3275));
#698=EDGE_LOOP('',(#3276));
#699=EDGE_LOOP('',(#3277));
#700=EDGE_LOOP('',(#3278));
#701=EDGE_LOOP('',(#3279));
#1037=LINE('',#5891,#1416);
#1038=LINE('',#5897,#1417);
#1039=LINE('',#5903,#1418);
#1040=LINE('',#5909,#1419);
#1041=LINE('',#5914,#1420);
#1042=LINE('',#5916,#1421);
#1043=LINE('',#5918,#1422);
#1044=LINE('',#5919,#1423);
#1045=LINE('',#5922,#1424);
#1046=LINE('',#5924,#1425);
#1047=LINE('',#5925,#1426);
#1048=LINE('',#5928,#1427);
#1049=LINE('',#5930,#1428);
#1050=LINE('',#5931,#1429);
#1051=LINE('',#5934,#1430);
#1052=LINE('',#5936,#1431);
#1053=LINE('',#5937,#1432);
#1054=LINE('',#5940,#1433);
#1055=LINE('',#5942,#1434);
#1056=LINE('',#5943,#1435);
#1057=LINE('',#5946,#1436);
#1058=LINE('',#5948,#1437);
#1059=LINE('',#5949,#1438);
#1060=LINE('',#5952,#1439);
#1061=LINE('',#5954,#1440);
#1062=LINE('',#5955,#1441);
#1063=LINE('',#5958,#1442);
#1064=LINE('',#5960,#1443);
#1065=LINE('',#5961,#1444);
#1066=LINE('',#5964,#1445);
#1067=LINE('',#5966,#1446);
#1068=LINE('',#5967,#1447);
#1069=LINE('',#5969,#1448);
#1070=LINE('',#5970,#1449);
#1416=VECTOR('',#4872,1.99999999999999);
#1417=VECTOR('',#4879,1.99999999999999);
#1418=VECTOR('',#4886,1.99999999999999);
#1419=VECTOR('',#4893,1.99999999999999);
#1420=VECTOR('',#4898,10.);
#1421=VECTOR('',#4899,10.);
#1422=VECTOR('',#4900,10.);
#1423=VECTOR('',#4901,10.);
#1424=VECTOR('',#4904,10.);
#1425=VECTOR('',#4905,10.);
#1426=VECTOR('',#4906,10.);
#1427=VECTOR('',#4909,10.);
#1428=VECTOR('',#4910,10.);
#1429=VECTOR('',#4911,10.);
#1430=VECTOR('',#4914,10.);
#1431=VECTOR('',#4915,10.);
#1432=VECTOR('',#4916,10.);
#1433=VECTOR('',#4919,10.);
#1434=VECTOR('',#4920,10.);
#1435=VECTOR('',#4921,10.);
#1436=VECTOR('',#4924,10.);
#1437=VECTOR('',#4925,10.);
#1438=VECTOR('',#4926,10.);
#1439=VECTOR('',#4929,10.);
#1440=VECTOR('',#4930,10.);
#1441=VECTOR('',#4931,10.);
#1442=VECTOR('',#4934,10.);
#1443=VECTOR('',#4935,10.);
#1444=VECTOR('',#4936,10.);
#1445=VECTOR('',#4939,10.);
#1446=VECTOR('',#4940,10.);
#1447=VECTOR('',#4941,10.);
#1448=VECTOR('',#4944,10.);
#1449=VECTOR('',#4945,10.);
#1574=CIRCLE('',#3984,1.99999999999999);
#1575=CIRCLE('',#3985,1.99999999999999);
#1576=CIRCLE('',#3987,1.99999999999999);
#1577=CIRCLE('',#3988,1.99999999999999);
#1578=CIRCLE('',#3990,1.99999999999999);
#1579=CIRCLE('',#3991,1.99999999999999);
#1580=CIRCLE('',#3993,1.99999999999999);
#1581=CIRCLE('',#3994,1.99999999999999);
#1853=VERTEX_POINT('',#5888);
#1854=VERTEX_POINT('',#5890);
#1855=VERTEX_POINT('',#5894);
#1856=VERTEX_POINT('',#5896);
#1857=VERTEX_POINT('',#5900);
#1858=VERTEX_POINT('',#5902);
#1859=VERTEX_POINT('',#5906);
#1860=VERTEX_POINT('',#5908);
#1861=VERTEX_POINT('',#5912);
#1862=VERTEX_POINT('',#5913);
#1863=VERTEX_POINT('',#5915);
#1864=VERTEX_POINT('',#5917);
#1865=VERTEX_POINT('',#5921);
#1866=VERTEX_POINT('',#5923);
#1867=VERTEX_POINT('',#5927);
#1868=VERTEX_POINT('',#5929);
#1869=VERTEX_POINT('',#5933);
#1870=VERTEX_POINT('',#5935);
#1871=VERTEX_POINT('',#5939);
#1872=VERTEX_POINT('',#5941);
#1873=VERTEX_POINT('',#5945);
#1874=VERTEX_POINT('',#5947);
#1875=VERTEX_POINT('',#5951);
#1876=VERTEX_POINT('',#5953);
#1877=VERTEX_POINT('',#5957);
#1878=VERTEX_POINT('',#5959);
#1879=VERTEX_POINT('',#5963);
#1880=VERTEX_POINT('',#5965);
#2310=EDGE_CURVE('',#1853,#1853,#1574,.T.);
#2311=EDGE_CURVE('',#1853,#1854,#1037,.T.);
#2312=EDGE_CURVE('',#1854,#1854,#1575,.T.);
#2313=EDGE_CURVE('',#1855,#1855,#1576,.T.);
#2314=EDGE_CURVE('',#1855,#1856,#1038,.T.);
#2315=EDGE_CURVE('',#1856,#1856,#1577,.T.);
#2316=EDGE_CURVE('',#1857,#1857,#1578,.T.);
#2317=EDGE_CURVE('',#1857,#1858,#1039,.T.);
#2318=EDGE_CURVE('',#1858,#1858,#1579,.T.);
#2319=EDGE_CURVE('',#1859,#1859,#1580,.T.);
#2320=EDGE_CURVE('',#1859,#1860,#1040,.T.);
#2321=EDGE_CURVE('',#1860,#1860,#1581,.T.);
#2322=EDGE_CURVE('',#1861,#1862,#1041,.T.);
#2323=EDGE_CURVE('',#1861,#1863,#1042,.T.);
#2324=EDGE_CURVE('',#1863,#1864,#1043,.T.);
#2325=EDGE_CURVE('',#1862,#1864,#1044,.T.);
#2326=EDGE_CURVE('',#1865,#1861,#1045,.T.);
#2327=EDGE_CURVE('',#1865,#1866,#1046,.T.);
#2328=EDGE_CURVE('',#1866,#1863,#1047,.T.);
#2329=EDGE_CURVE('',#1867,#1865,#1048,.T.);
#2330=EDGE_CURVE('',#1867,#1868,#1049,.T.);
#2331=EDGE_CURVE('',#1868,#1866,#1050,.T.);
#2332=EDGE_CURVE('',#1869,#1867,#1051,.T.);
#2333=EDGE_CURVE('',#1869,#1870,#1052,.T.);
#2334=EDGE_CURVE('',#1870,#1868,#1053,.T.);
#2335=EDGE_CURVE('',#1871,#1869,#1054,.T.);
#2336=EDGE_CURVE('',#1871,#1872,#1055,.T.);
#2337=EDGE_CURVE('',#1872,#1870,#1056,.T.);
#2338=EDGE_CURVE('',#1873,#1871,#1057,.T.);
#2339=EDGE_CURVE('',#1873,#1874,#1058,.T.);
#2340=EDGE_CURVE('',#1874,#1872,#1059,.T.);
#2341=EDGE_CURVE('',#1875,#1873,#1060,.T.);
#2342=EDGE_CURVE('',#1875,#1876,#1061,.T.);
#2343=EDGE_CURVE('',#1876,#1874,#1062,.T.);
#2344=EDGE_CURVE('',#1877,#1875,#1063,.T.);
#2345=EDGE_CURVE('',#1877,#1878,#1064,.T.);
#2346=EDGE_CURVE('',#1878,#1876,#1065,.T.);
#2347=EDGE_CURVE('',#1879,#1877,#1066,.T.);
#2348=EDGE_CURVE('',#1879,#1880,#1067,.T.);
#2349=EDGE_CURVE('',#1880,#1878,#1068,.T.);
#2350=EDGE_CURVE('',#1862,#1879,#1069,.T.);
#2351=EDGE_CURVE('',#1864,#1880,#1070,.T.);
#3196=ORIENTED_EDGE('',*,*,#2310,.T.);
#3197=ORIENTED_EDGE('',*,*,#2311,.T.);
#3198=ORIENTED_EDGE('',*,*,#2312,.F.);
#3199=ORIENTED_EDGE('',*,*,#2311,.F.);
#3200=ORIENTED_EDGE('',*,*,#2313,.T.);
#3201=ORIENTED_EDGE('',*,*,#2314,.T.);
#3202=ORIENTED_EDGE('',*,*,#2315,.F.);
#3203=ORIENTED_EDGE('',*,*,#2314,.F.);
#3204=ORIENTED_EDGE('',*,*,#2316,.T.);
#3205=ORIENTED_EDGE('',*,*,#2317,.T.);
#3206=ORIENTED_EDGE('',*,*,#2318,.F.);
#3207=ORIENTED_EDGE('',*,*,#2317,.F.);
#3208=ORIENTED_EDGE('',*,*,#2319,.T.);
#3209=ORIENTED_EDGE('',*,*,#2320,.T.);
#3210=ORIENTED_EDGE('',*,*,#2321,.F.);
#3211=ORIENTED_EDGE('',*,*,#2320,.F.);
#3212=ORIENTED_EDGE('',*,*,#2322,.F.);
#3213=ORIENTED_EDGE('',*,*,#2323,.T.);
#3214=ORIENTED_EDGE('',*,*,#2324,.T.);
#3215=ORIENTED_EDGE('',*,*,#2325,.F.);
#3216=ORIENTED_EDGE('',*,*,#2326,.F.);
#3217=ORIENTED_EDGE('',*,*,#2327,.T.);
#3218=ORIENTED_EDGE('',*,*,#2328,.T.);
#3219=ORIENTED_EDGE('',*,*,#2323,.F.);
#3220=ORIENTED_EDGE('',*,*,#2329,.F.);
#3221=ORIENTED_EDGE('',*,*,#2330,.T.);
#3222=ORIENTED_EDGE('',*,*,#2331,.T.);
#3223=ORIENTED_EDGE('',*,*,#2327,.F.);
#3224=ORIENTED_EDGE('',*,*,#2332,.F.);
#3225=ORIENTED_EDGE('',*,*,#2333,.T.);
#3226=ORIENTED_EDGE('',*,*,#2334,.T.);
#3227=ORIENTED_EDGE('',*,*,#2330,.F.);
#3228=ORIENTED_EDGE('',*,*,#2335,.F.);
#3229=ORIENTED_EDGE('',*,*,#2336,.T.);
#3230=ORIENTED_EDGE('',*,*,#2337,.T.);
#3231=ORIENTED_EDGE('',*,*,#2333,.F.);
#3232=ORIENTED_EDGE('',*,*,#2338,.F.);
#3233=ORIENTED_EDGE('',*,*,#2339,.T.);
#3234=ORIENTED_EDGE('',*,*,#2340,.T.);
#3235=ORIENTED_EDGE('',*,*,#2336,.F.);
#3236=ORIENTED_EDGE('',*,*,#2341,.F.);
#3237=ORIENTED_EDGE('',*,*,#2342,.T.);
#3238=ORIENTED_EDGE('',*,*,#2343,.T.);
#3239=ORIENTED_EDGE('',*,*,#2339,.F.);
#3240=ORIENTED_EDGE('',*,*,#2344,.F.);
#3241=ORIENTED_EDGE('',*,*,#2345,.T.);
#3242=ORIENTED_EDGE('',*,*,#2346,.T.);
#3243=ORIENTED_EDGE('',*,*,#2342,.F.);
#3244=ORIENTED_EDGE('',*,*,#2347,.F.);
#3245=ORIENTED_EDGE('',*,*,#2348,.T.);
#3246=ORIENTED_EDGE('',*,*,#2349,.T.);
#3247=ORIENTED_EDGE('',*,*,#2345,.F.);
#3248=ORIENTED_EDGE('',*,*,#2350,.F.);
#3249=ORIENTED_EDGE('',*,*,#2325,.T.);
#3250=ORIENTED_EDGE('',*,*,#2351,.T.);
#3251=ORIENTED_EDGE('',*,*,#2348,.F.);
#3252=ORIENTED_EDGE('',*,*,#2351,.F.);
#3253=ORIENTED_EDGE('',*,*,#2324,.F.);
#3254=ORIENTED_EDGE('',*,*,#2328,.F.);
#3255=ORIENTED_EDGE('',*,*,#2331,.F.);
#3256=ORIENTED_EDGE('',*,*,#2334,.F.);
#3257=ORIENTED_EDGE('',*,*,#2337,.F.);
#3258=ORIENTED_EDGE('',*,*,#2340,.F.);
#3259=ORIENTED_EDGE('',*,*,#2343,.F.);
#3260=ORIENTED_EDGE('',*,*,#2346,.F.);
#3261=ORIENTED_EDGE('',*,*,#2349,.F.);
#3262=ORIENTED_EDGE('',*,*,#2319,.F.);
#3263=ORIENTED_EDGE('',*,*,#2316,.F.);
#3264=ORIENTED_EDGE('',*,*,#2313,.F.);
#3265=ORIENTED_EDGE('',*,*,#2310,.F.);
#3266=ORIENTED_EDGE('',*,*,#2350,.T.);
#3267=ORIENTED_EDGE('',*,*,#2347,.T.);
#3268=ORIENTED_EDGE('',*,*,#2344,.T.);
#3269=ORIENTED_EDGE('',*,*,#2341,.T.);
#3270=ORIENTED_EDGE('',*,*,#2338,.T.);
#3271=ORIENTED_EDGE('',*,*,#2335,.T.);
#3272=ORIENTED_EDGE('',*,*,#2332,.T.);
#3273=ORIENTED_EDGE('',*,*,#2329,.T.);
#3274=ORIENTED_EDGE('',*,*,#2326,.T.);
#3275=ORIENTED_EDGE('',*,*,#2322,.T.);
#3276=ORIENTED_EDGE('',*,*,#2321,.T.);
#3277=ORIENTED_EDGE('',*,*,#2318,.T.);
#3278=ORIENTED_EDGE('',*,*,#2315,.T.);
#3279=ORIENTED_EDGE('',*,*,#2312,.T.);
#3397=CYLINDRICAL_SURFACE('',#3983,1.99999999999999);
#3398=CYLINDRICAL_SURFACE('',#3986,1.99999999999999);
#3399=CYLINDRICAL_SURFACE('',#3989,1.99999999999999);
#3400=CYLINDRICAL_SURFACE('',#3992,1.99999999999999);
#3561=ADVANCED_FACE('',(#454),#3397,.F.);
#3562=ADVANCED_FACE('',(#455),#3398,.F.);
#3563=ADVANCED_FACE('',(#456),#3399,.F.);
#3564=ADVANCED_FACE('',(#457),#3400,.F.);
#3565=ADVANCED_FACE('',(#458),#274,.F.);
#3566=ADVANCED_FACE('',(#459),#275,.F.);
#3567=ADVANCED_FACE('',(#460),#276,.F.);
#3568=ADVANCED_FACE('',(#461),#277,.F.);
#3569=ADVANCED_FACE('',(#462),#278,.F.);
#3570=ADVANCED_FACE('',(#463),#279,.F.);
#3571=ADVANCED_FACE('',(#464),#280,.F.);
#3572=ADVANCED_FACE('',(#465),#281,.F.);
#3573=ADVANCED_FACE('',(#466),#282,.F.);
#3574=ADVANCED_FACE('',(#467),#283,.F.);
#3575=ADVANCED_FACE('',(#468,#142,#143,#144,#145),#284,.F.);
#3576=ADVANCED_FACE('',(#469,#146,#147,#148,#149),#285,.T.);
#3602=CLOSED_SHELL('',(#3561,#3562,#3563,#3564,#3565,#3566,#3567,#3568,
#3569,#3570,#3571,#3572,#3573,#3574,#3575,#3576));
#3982=AXIS2_PLACEMENT_3D('',#5886,#4866,#4867);
#3983=AXIS2_PLACEMENT_3D('',#5887,#4868,#4869);
#3984=AXIS2_PLACEMENT_3D('',#5889,#4870,#4871);
#3985=AXIS2_PLACEMENT_3D('',#5892,#4873,#4874);
#3986=AXIS2_PLACEMENT_3D('',#5893,#4875,#4876);
#3987=AXIS2_PLACEMENT_3D('',#5895,#4877,#4878);
#3988=AXIS2_PLACEMENT_3D('',#5898,#4880,#4881);
#3989=AXIS2_PLACEMENT_3D('',#5899,#4882,#4883);
#3990=AXIS2_PLACEMENT_3D('',#5901,#4884,#4885);
#3991=AXIS2_PLACEMENT_3D('',#5904,#4887,#4888);
#3992=AXIS2_PLACEMENT_3D('',#5905,#4889,#4890);
#3993=AXIS2_PLACEMENT_3D('',#5907,#4891,#4892);
#3994=AXIS2_PLACEMENT_3D('',#5910,#4894,#4895);
#3995=AXIS2_PLACEMENT_3D('',#5911,#4896,#4897);
#3996=AXIS2_PLACEMENT_3D('',#5920,#4902,#4903);
#3997=AXIS2_PLACEMENT_3D('',#5926,#4907,#4908);
#3998=AXIS2_PLACEMENT_3D('',#5932,#4912,#4913);
#3999=AXIS2_PLACEMENT_3D('',#5938,#4917,#4918);
#4000=AXIS2_PLACEMENT_3D('',#5944,#4922,#4923);
#4001=AXIS2_PLACEMENT_3D('',#5950,#4927,#4928);
#4002=AXIS2_PLACEMENT_3D('',#5956,#4932,#4933);
#4003=AXIS2_PLACEMENT_3D('',#5962,#4937,#4938);
#4004=AXIS2_PLACEMENT_3D('',#5968,#4942,#4943);
#4005=AXIS2_PLACEMENT_3D('',#5971,#4946,#4947);
#4006=AXIS2_PLACEMENT_3D('',#5972,#4948,#4949);
#4866=DIRECTION('axis',(0.,0.,1.));
#4867=DIRECTION('refdir',(1.,0.,0.));
#4868=DIRECTION('center_axis',(0.,-1.,0.));
#4869=DIRECTION('ref_axis',(1.,0.,0.));
#4870=DIRECTION('center_axis',(0.,1.,0.));
#4871=DIRECTION('ref_axis',(1.,0.,0.));
#4872=DIRECTION('',(0.,-1.,0.));
#4873=DIRECTION('center_axis',(0.,1.,0.));
#4874=DIRECTION('ref_axis',(1.,0.,0.));
#4875=DIRECTION('center_axis',(0.,-1.,0.));
#4876=DIRECTION('ref_axis',(1.,0.,0.));
#4877=DIRECTION('center_axis',(0.,1.,0.));
#4878=DIRECTION('ref_axis',(1.,0.,0.));
#4879=DIRECTION('',(0.,-1.,0.));
#4880=DIRECTION('center_axis',(0.,1.,0.));
#4881=DIRECTION('ref_axis',(1.,0.,0.));
#4882=DIRECTION('center_axis',(0.,-1.,0.));
#4883=DIRECTION('ref_axis',(1.,0.,0.));
#4884=DIRECTION('center_axis',(0.,1.,0.));
#4885=DIRECTION('ref_axis',(1.,0.,0.));
#4886=DIRECTION('',(0.,-1.,0.));
#4887=DIRECTION('center_axis',(0.,1.,0.));
#4888=DIRECTION('ref_axis',(1.,0.,0.));
#4889=DIRECTION('center_axis',(0.,-1.,0.));
#4890=DIRECTION('ref_axis',(1.,0.,0.));
#4891=DIRECTION('center_axis',(0.,1.,0.));
#4892=DIRECTION('ref_axis',(1.,0.,0.));
#4893=DIRECTION('',(0.,-1.,0.));
#4894=DIRECTION('center_axis',(0.,1.,0.));
#4895=DIRECTION('ref_axis',(1.,0.,0.));
#4896=DIRECTION('center_axis',(0.,0.,1.));
#4897=DIRECTION('ref_axis',(1.,0.,0.));
#4898=DIRECTION('',(1.,0.,0.));
#4899=DIRECTION('',(0.,1.,0.));
#4900=DIRECTION('',(1.,0.,0.));
#4901=DIRECTION('',(0.,1.,0.));
#4902=DIRECTION('center_axis',(-1.,0.,0.));
#4903=DIRECTION('ref_axis',(0.,0.,1.));
#4904=DIRECTION('',(0.,0.,1.));
#4905=DIRECTION('',(0.,1.,0.));
#4906=DIRECTION('',(0.,0.,1.));
#4907=DIRECTION('center_axis',(0.,0.,-1.));
#4908=DIRECTION('ref_axis',(-1.,0.,0.));
#4909=DIRECTION('',(-1.,0.,0.));
#4910=DIRECTION('',(0.,1.,0.));
#4911=DIRECTION('',(-1.,0.,0.));
#4912=DIRECTION('center_axis',(-1.,0.,0.));
#4913=DIRECTION('ref_axis',(0.,0.,1.));
#4914=DIRECTION('',(0.,0.,1.));
#4915=DIRECTION('',(0.,1.,0.));
#4916=DIRECTION('',(0.,0.,1.));
#4917=DIRECTION('center_axis',(0.,0.,1.));
#4918=DIRECTION('ref_axis',(1.,0.,0.));
#4919=DIRECTION('',(1.,0.,0.));
#4920=DIRECTION('',(0.,1.,0.));
#4921=DIRECTION('',(1.,0.,0.));
#4922=DIRECTION('center_axis',(1.,0.,0.));
#4923=DIRECTION('ref_axis',(0.,0.,-1.));
#4924=DIRECTION('',(0.,0.,-1.));
#4925=DIRECTION('',(0.,1.,0.));
#4926=DIRECTION('',(0.,0.,-1.));
#4927=DIRECTION('center_axis',(0.,0.,-1.));
#4928=DIRECTION('ref_axis',(-1.,0.,0.));
#4929=DIRECTION('',(-1.,0.,0.));
#4930=DIRECTION('',(0.,1.,0.));
#4931=DIRECTION('',(-1.,0.,0.));
#4932=DIRECTION('center_axis',(-1.,0.,0.));
#4933=DIRECTION('ref_axis',(0.,0.,1.));
#4934=DIRECTION('',(0.,0.,1.));
#4935=DIRECTION('',(0.,1.,0.));
#4936=DIRECTION('',(0.,0.,1.));
#4937=DIRECTION('center_axis',(0.,0.,1.));
#4938=DIRECTION('ref_axis',(1.,0.,0.));
#4939=DIRECTION('',(1.,0.,0.));
#4940=DIRECTION('',(0.,1.,0.));
#4941=DIRECTION('',(1.,0.,0.));
#4942=DIRECTION('center_axis',(1.,0.,0.));
#4943=DIRECTION('ref_axis',(0.,0.,-1.));
#4944=DIRECTION('',(0.,0.,-1.));
#4945=DIRECTION('',(0.,0.,-1.));
#4946=DIRECTION('center_axis',(0.,-1.,0.));
#4947=DIRECTION('ref_axis',(1.,0.,0.));
#4948=DIRECTION('center_axis',(0.,-1.,0.));
#4949=DIRECTION('ref_axis',(1.,0.,0.));
#5886=CARTESIAN_POINT('',(0.,0.,0.));
#5887=CARTESIAN_POINT('Origin',(-31.6092837386808,460.5,108.939950998448));
#5888=CARTESIAN_POINT('',(-33.6092837386808,463.5,108.939950998448));
#5889=CARTESIAN_POINT('Origin',(-31.6092837386808,463.5,108.939950998448));
#5890=CARTESIAN_POINT('',(-33.6092837386808,460.5,108.939950998448));
#5891=CARTESIAN_POINT('',(-33.6092837386808,460.5,108.939950998448));
#5892=CARTESIAN_POINT('Origin',(-31.6092837386808,460.5,108.939950998448));
#5893=CARTESIAN_POINT('Origin',(-71.0061608111161,460.5,95.0000000000015));
#5894=CARTESIAN_POINT('',(-73.0061608111161,463.5,95.0000000000015));
#5895=CARTESIAN_POINT('Origin',(-71.0061608111161,463.5,95.0000000000015));
#5896=CARTESIAN_POINT('',(-73.0061608111161,460.5,95.0000000000015));
#5897=CARTESIAN_POINT('',(-73.0061608111161,460.5,95.0000000000015));
#5898=CARTESIAN_POINT('Origin',(-71.0061608111161,460.5,95.0000000000015));
#5899=CARTESIAN_POINT('Origin',(-28.0061608111161,460.5,95.0000000000015));
#5900=CARTESIAN_POINT('',(-30.0061608111161,463.5,95.0000000000015));
#5901=CARTESIAN_POINT('Origin',(-28.0061608111161,463.5,95.0000000000015));
#5902=CARTESIAN_POINT('',(-30.0061608111161,460.5,95.0000000000015));
#5903=CARTESIAN_POINT('',(-30.0061608111161,460.5,95.0000000000015));
#5904=CARTESIAN_POINT('Origin',(-28.0061608111161,460.5,95.0000000000015));
#5905=CARTESIAN_POINT('Origin',(-67.4030378835514,460.5,108.939950998448));
#5906=CARTESIAN_POINT('',(-69.4030378835514,463.5,108.939950998448));
#5907=CARTESIAN_POINT('Origin',(-67.4030378835514,463.5,108.939950998448));
#5908=CARTESIAN_POINT('',(-69.4030378835514,460.5,108.939950998448));
#5909=CARTESIAN_POINT('',(-69.4030378835514,460.5,108.939950998448));
#5910=CARTESIAN_POINT('Origin',(-67.4030378835514,460.5,108.939950998448));
#5911=CARTESIAN_POINT('Origin',(-67.5061608111161,460.5,105.000000000001));
#5912=CARTESIAN_POINT('',(-67.5061608111161,460.5,105.000000000001));
#5913=CARTESIAN_POINT('',(-31.5061608111161,460.5,105.000000000001));
#5914=CARTESIAN_POINT('',(-67.5061608111161,460.5,105.000000000001));
#5915=CARTESIAN_POINT('',(-67.5061608111161,463.5,105.000000000001));
#5916=CARTESIAN_POINT('',(-67.5061608111161,460.5,105.000000000001));
#5917=CARTESIAN_POINT('',(-31.5061608111161,463.5,105.000000000001));
#5918=CARTESIAN_POINT('',(-67.5061608111161,463.5,105.000000000001));
#5919=CARTESIAN_POINT('',(-31.5061608111161,460.5,105.000000000001));
#5920=CARTESIAN_POINT('Origin',(-67.5061608111161,460.5,85.0000000000015));
#5921=CARTESIAN_POINT('',(-67.5061608111161,460.5,85.0000000000015));
#5922=CARTESIAN_POINT('',(-67.5061608111161,460.5,85.0000000000015));
#5923=CARTESIAN_POINT('',(-67.5061608111161,463.5,85.0000000000015));
#5924=CARTESIAN_POINT('',(-67.5061608111161,460.5,85.0000000000015));
#5925=CARTESIAN_POINT('',(-67.5061608111161,463.5,85.0000000000015));
#5926=CARTESIAN_POINT('Origin',(-51.5061608111161,460.5,85.0000000000015));
#5927=CARTESIAN_POINT('',(-51.5061608111161,460.5,85.0000000000015));
#5928=CARTESIAN_POINT('',(-31.5061608111161,460.5,85.0000000000015));
#5929=CARTESIAN_POINT('',(-51.5061608111161,463.5,85.0000000000015));
#5930=CARTESIAN_POINT('',(-51.5061608111161,460.5,85.0000000000015));
#5931=CARTESIAN_POINT('',(-31.5061608111161,463.5,85.0000000000015));
#5932=CARTESIAN_POINT('Origin',(-51.5061608111161,460.5,77.5000000000015));
#5933=CARTESIAN_POINT('',(-51.5061608111161,460.5,77.5000000000015));
#5934=CARTESIAN_POINT('',(-51.5061608111161,460.5,65.0000000000015));
#5935=CARTESIAN_POINT('',(-51.5061608111161,463.5,77.5000000000015));
#5936=CARTESIAN_POINT('',(-51.5061608111161,460.5,77.5000000000015));
#5937=CARTESIAN_POINT('',(-51.5061608111161,463.5,65.0000000000015));
#5938=CARTESIAN_POINT('Origin',(-74.5061608111161,460.5,77.5000000000015));
#5939=CARTESIAN_POINT('',(-74.5061608111161,460.5,77.5000000000015));
#5940=CARTESIAN_POINT('',(-74.5061608111161,460.5,77.5000000000015));
#5941=CARTESIAN_POINT('',(-74.5061608111161,463.5,77.5000000000015));
#5942=CARTESIAN_POINT('',(-74.5061608111161,460.5,77.5000000000015));
#5943=CARTESIAN_POINT('',(-74.5061608111161,463.5,77.5000000000015));
#5944=CARTESIAN_POINT('Origin',(-74.5061608111161,460.5,112.500000000001));
#5945=CARTESIAN_POINT('',(-74.5061608111161,460.5,112.500000000001));
#5946=CARTESIAN_POINT('',(-74.5061608111161,460.5,112.500000000001));
#5947=CARTESIAN_POINT('',(-74.5061608111161,463.5,112.500000000001));
#5948=CARTESIAN_POINT('',(-74.5061608111161,460.5,112.500000000001));
#5949=CARTESIAN_POINT('',(-74.5061608111161,463.5,112.500000000001));
#5950=CARTESIAN_POINT('Origin',(-24.5061608111161,460.5,112.500000000001));
#5951=CARTESIAN_POINT('',(-24.5061608111161,460.5,112.500000000001));
#5952=CARTESIAN_POINT('',(-24.5061608111161,460.5,112.500000000001));
#5953=CARTESIAN_POINT('',(-24.5061608111161,463.5,112.500000000001));
#5954=CARTESIAN_POINT('',(-24.5061608111161,460.5,112.500000000001));
#5955=CARTESIAN_POINT('',(-24.5061608111161,463.5,112.500000000001));
#5956=CARTESIAN_POINT('Origin',(-24.5061608111161,460.5,77.5000000000015));
#5957=CARTESIAN_POINT('',(-24.5061608111161,460.5,77.5000000000015));
#5958=CARTESIAN_POINT('',(-24.5061608111161,460.5,77.5000000000015));
#5959=CARTESIAN_POINT('',(-24.5061608111161,463.5,77.5000000000015));
#5960=CARTESIAN_POINT('',(-24.5061608111161,460.5,77.5000000000015));
#5961=CARTESIAN_POINT('',(-24.5061608111161,463.5,77.5000000000015));
#5962=CARTESIAN_POINT('Origin',(-31.5061608111161,460.5,77.5000000000015));
#5963=CARTESIAN_POINT('',(-31.5061608111161,460.5,77.5000000000015));
#5964=CARTESIAN_POINT('',(-74.5061608111161,460.5,77.5000000000015));
#5965=CARTESIAN_POINT('',(-31.5061608111161,463.5,77.5000000000015));
#5966=CARTESIAN_POINT('',(-31.5061608111161,460.5,77.5000000000015));
#5967=CARTESIAN_POINT('',(-74.5061608111161,463.5,77.5000000000015));
#5968=CARTESIAN_POINT('Origin',(-31.5061608111161,460.5,105.000000000001));
#5969=CARTESIAN_POINT('',(-31.5061608111161,460.5,85.0000000000015));
#5970=CARTESIAN_POINT('',(-31.5061608111161,463.5,85.0000000000015));
#5971=CARTESIAN_POINT('Origin',(-49.5061608111161,463.5,95.0000000000015));
#5972=CARTESIAN_POINT('Origin',(-49.5061608111161,460.5,95.0000000000015));
#6081=UNCERTAINTY_MEASURE_WITH_UNIT(LENGTH_MEASURE(0.01),#6097,
'DISTANCE_ACCURACY_VALUE',
'Maximum model space distance between geometric entities at asserted c
onnectivities');
#6083=UNCERTAINTY_MEASURE_WITH_UNIT(LENGTH_MEASURE(0.01),#6097,
'DISTANCE_ACCURACY_VALUE',
'Maximum model space distance between geometric entities at asserted c
onnectivities');
#6094=(
GEOMETRIC_REPRESENTATION_CONTEXT(3)
GLOBAL_UNCERTAINTY_ASSIGNED_CONTEXT((#6081))
GLOBAL_UNIT_ASSIGNED_CONTEXT((#6097,#6099,#6100))
REPRESENTATION_CONTEXT('','3D')
);
#6096=(
GEOMETRIC_REPRESENTATION_CONTEXT(3)
GLOBAL_UNCERTAINTY_ASSIGNED_CONTEXT((#6083))
GLOBAL_UNIT_ASSIGNED_CONTEXT((#6097,#6099,#6100))
REPRESENTATION_CONTEXT('','3D')
);
#6097=(
LENGTH_UNIT()
NAMED_UNIT(*)
SI_UNIT(.MILLI.,.METRE.)
);
#6099=(
NAMED_UNIT(*)
PLANE_ANGLE_UNIT()
SI_UNIT($,.RADIAN.)
);
#6100=(
NAMED_UNIT(*)
SI_UNIT($,.STERADIAN.)
SOLID_ANGLE_UNIT()
);
#6111=SHAPE_DEFINITION_REPRESENTATION(#6123,#6146);
#6123=PRODUCT_DEFINITION_SHAPE('',$,#6159);
#6146=SHAPE_REPRESENTATION('',(#3982),#6094);
#6148=PRODUCT_DEFINITION_CONTEXT('part definition',#6186,'design');
#6159=PRODUCT_DEFINITION('Bracket_03','Bracket_03',#6171,#6148);
#6171=PRODUCT_DEFINITION_FORMATION('',$,#6198);
#6186=APPLICATION_CONTEXT(
'Core Data for Automotive Mechanical Design Process');
#6187=PRODUCT_CONTEXT('part definition',#6186,'mechanical');
#6198=PRODUCT('Bracket_03','Bracket_03',$,(#6187));
#6228=COLOUR_RGB('Dark Blue',0.08,0.2,0.34);
#6229=FILL_AREA_STYLE_COLOUR('',#6228);
#6230=FILL_AREA_STYLE('',(#6229));
#6231=SURFACE_STYLE_FILL_AREA(#6230);
#6232=SURFACE_SIDE_STYLE('',(#6231));
#6233=SURFACE_STYLE_USAGE(.BOTH.,#6232);
#6234=PRESENTATION_STYLE_ASSIGNMENT((#6233));
ENDSEC;
END-ISO-10303-21;
